ISO-10303-21;
HEADER;
/* Generated by software containing ST-Developer
 * from STEP Tools, Inc. (www.steptools.com) 
 */

FILE_DESCRIPTION(
/* description */ ('Bin tilter linkage'),
/* implementation_level */ '2;1');

FILE_NAME(
/* name */ 'M4 short cap screw (24).step',
/* time_stamp */ '2026-10-28T03:26:24-07:00',
/* author */ (''),
/* organization */ (''),
/* preprocessor_version */ 'ST-DEVELOPER v20.2',
/* originating_system */ 'Autodesk Translation Framework v15.17.0.0',
/* authorisation */ '');

FILE_SCHEMA (('AUTOMOTIVE_DESIGN { 1 0 10303 214 3 1 1 }'));
ENDSEC;

DATA;
#10=MECHANICAL_DESIGN_GEOMETRIC_PRESENTATION_REPRESENTATION('',(#925),#23728);
#713=SHAPE_REPRESENTATION_RELATIONSHIP('SRR','None',#24179,#819);
#819=ADVANCED_BREP_SHAPE_REPRESENTATION('',(#1038),#23679);
#925=STYLED_ITEM('',(#24772),#1038);
#1038=MANIFOLD_SOLID_BREP('Body1',#12456);
#1368=FACE_BOUND('',#3406,.T.);
#1711=PLANE('',#14673);
#1712=PLANE('',#14678);
#1713=PLANE('',#14681);
#2347=FACE_OUTER_BOUND('',#3405,.T.);
#2348=FACE_OUTER_BOUND('',#3407,.T.);
#2349=FACE_OUTER_BOUND('',#3408,.T.);
#2350=FACE_OUTER_BOUND('',#3409,.T.);
#2351=FACE_OUTER_BOUND('',#3410,.T.);
#3405=EDGE_LOOP('',(#10081));
#3406=EDGE_LOOP('',(#10082));
#3407=EDGE_LOOP('',(#10083,#10084,#10085,#10086));
#3408=EDGE_LOOP('',(#10087));
#3409=EDGE_LOOP('',(#10088,#10089,#10090,#10091));
#3410=EDGE_LOOP('',(#10092));
#4231=LINE('',#21699,#4906);
#4232=LINE('',#21705,#4907);
#4906=VECTOR('',#17858,0.350000000000001);
#4907=VECTOR('',#17867,0.199999999999999);
#5671=CIRCLE('',#14674,0.350000000000001);
#5672=CIRCLE('',#14675,0.199999999999999);
#5673=CIRCLE('',#14677,0.350000000000001);
#5674=CIRCLE('',#14680,0.199999999999999);
#6525=VERTEX_POINT('',#21693);
#6526=VERTEX_POINT('',#21695);
#6527=VERTEX_POINT('',#21698);
#6528=VERTEX_POINT('',#21703);
#7780=EDGE_CURVE('',#6525,#6525,#5671,.T.);
#7781=EDGE_CURVE('',#6526,#6526,#5672,.T.);
#7782=EDGE_CURVE('',#6525,#6527,#4231,.T.);
#7783=EDGE_CURVE('',#6527,#6527,#5673,.T.);
#7784=EDGE_CURVE('',#6528,#6528,#5674,.T.);
#7785=EDGE_CURVE('',#6528,#6526,#4232,.T.);
#10081=ORIENTED_EDGE('',*,*,#7780,.T.);
#10082=ORIENTED_EDGE('',*,*,#7781,.F.);
#10083=ORIENTED_EDGE('',*,*,#7780,.F.);
#10084=ORIENTED_EDGE('',*,*,#7782,.T.);
#10085=ORIENTED_EDGE('',*,*,#7783,.T.);
#10086=ORIENTED_EDGE('',*,*,#7782,.F.);
#10087=ORIENTED_EDGE('',*,*,#7783,.F.);
#10088=ORIENTED_EDGE('',*,*,#7784,.F.);
#10089=ORIENTED_EDGE('',*,*,#7785,.T.);
#10090=ORIENTED_EDGE('',*,*,#7781,.T.);
#10091=ORIENTED_EDGE('',*,*,#7785,.F.);
#10092=ORIENTED_EDGE('',*,*,#7784,.T.);
#11501=CYLINDRICAL_SURFACE('',#14676,0.350000000000001);
#11502=CYLINDRICAL_SURFACE('',#14679,0.199999999999999);
#12072=ADVANCED_FACE('',(#2347,#1368),#1711,.T.);
#12073=ADVANCED_FACE('',(#2348),#11501,.T.);
#12074=ADVANCED_FACE('',(#2349),#1712,.F.);
#12075=ADVANCED_FACE('',(#2350),#11502,.T.);
#12076=ADVANCED_FACE('',(#2351),#1713,.T.);
#12456=CLOSED_SHELL('',(#12072,#12073,#12074,#12075,#12076));
#14672=AXIS2_PLACEMENT_3D('',#21691,#17848,#17849);
#14673=AXIS2_PLACEMENT_3D('',#21692,#17850,#17851);
#14674=AXIS2_PLACEMENT_3D('',#21694,#17852,#17853);
#14675=AXIS2_PLACEMENT_3D('',#21696,#17854,#17855);
#14676=AXIS2_PLACEMENT_3D('',#21697,#17856,#17857);
#14677=AXIS2_PLACEMENT_3D('',#21700,#17859,#17860);
#14678=AXIS2_PLACEMENT_3D('',#21701,#17861,#17862);
#14679=AXIS2_PLACEMENT_3D('',#21702,#17863,#17864);
#14680=AXIS2_PLACEMENT_3D('',#21704,#17865,#17866);
#14681=AXIS2_PLACEMENT_3D('',#21706,#17868,#17869);
#17848=DIRECTION('axis',(0.,0.,1.));
#17849=DIRECTION('refdir',(1.,0.,0.));
#17850=DIRECTION('center_axis',(0.,1.,0.));
#17851=DIRECTION('ref_axis',(1.,0.,0.));
#17852=DIRECTION('center_axis',(0.,1.,0.));
#17853=DIRECTION('ref_axis',(1.,0.,0.));
#17854=DIRECTION('center_axis',(0.,1.,0.));
#17855=DIRECTION('ref_axis',(1.,0.,0.));
#17856=DIRECTION('center_axis',(0.,1.,0.));
#17857=DIRECTION('ref_axis',(1.,0.,0.));
#17858=DIRECTION('',(0.,-1.,0.));
#17859=DIRECTION('center_axis',(0.,1.,0.));
#17860=DIRECTION('ref_axis',(1.,0.,0.));
#17861=DIRECTION('center_axis',(0.,1.,0.));
#17862=DIRECTION('ref_axis',(1.,0.,0.));
#17863=DIRECTION('center_axis',(0.,1.,0.));
#17864=DIRECTION('ref_axis',(1.,0.,0.));
#17865=DIRECTION('center_axis',(0.,1.,0.));
#17866=DIRECTION('ref_axis',(1.,0.,0.));
#17867=DIRECTION('',(0.,-1.,0.));
#17868=DIRECTION('center_axis',(0.,1.,0.));
#17869=DIRECTION('ref_axis',(1.,0.,0.));
#21691=CARTESIAN_POINT('',(0.,0.,0.));
#21692=CARTESIAN_POINT('Origin',(25.5102260242172,-0.8,29.9659007476824));
#21693=CARTESIAN_POINT('',(25.1602260242172,-0.8,29.9659007476824));
#21694=CARTESIAN_POINT('Origin',(25.5102260242172,-0.8,29.9659007476824));
#21695=CARTESIAN_POINT('',(25.3102260242172,-0.8,29.9659007476824));
#21696=CARTESIAN_POINT('Origin',(25.5102260242172,-0.8,29.9659007476824));
#21697=CARTESIAN_POINT('Origin',(25.5102260242172,-1.2,29.9659007476824));
#21698=CARTESIAN_POINT('',(25.1602260242172,-1.2,29.9659007476824));
#21699=CARTESIAN_POINT('',(25.1602260242172,-1.2,29.9659007476824));
#21700=CARTESIAN_POINT('Origin',(25.5102260242172,-1.2,29.9659007476824));
#21701=CARTESIAN_POINT('Origin',(25.5102260242172,-1.2,29.9659007476824));
#21702=CARTESIAN_POINT('Origin',(25.5102260242172,-0.8,29.9659007476824));
#21703=CARTESIAN_POINT('',(25.3102260242172,-0.1,29.9659007476824));
#21704=CARTESIAN_POINT('Origin',(25.5102260242172,-0.1,29.9659007476824));
#21705=CARTESIAN_POINT('',(25.3102260242172,-0.8,29.9659007476824));
#21706=CARTESIAN_POINT('Origin',(25.5102260242172,-0.1,29.9659007476824));
#23562=UNCERTAINTY_MEASURE_WITH_UNIT(LENGTH_MEASURE(0.001),#23729,
'DISTANCE_ACCURACY_VALUE',
'Maximum model space distance between geometric entities at asserted c
onnectivities');
#23611=UNCERTAINTY_MEASURE_WITH_UNIT(LENGTH_MEASURE(0.001),#23729,
'DISTANCE_ACCURACY_VALUE',
'Maximum model space distance between geometric entities at asserted c
onnectivities');
#23679=(
GEOMETRIC_REPRESENTATION_CONTEXT(3)
GLOBAL_UNCERTAINTY_ASSIGNED_CONTEXT((#23562))
GLOBAL_UNIT_ASSIGNED_CONTEXT((#23729,#23731,#23732))
REPRESENTATION_CONTEXT('','3D')
);
#23728=(
GEOMETRIC_REPRESENTATION_CONTEXT(3)
GLOBAL_UNCERTAINTY_ASSIGNED_CONTEXT((#23611))
GLOBAL_UNIT_ASSIGNED_CONTEXT((#23729,#23731,#23732))
REPRESENTATION_CONTEXT('','3D')
);
#23729=(
LENGTH_UNIT()
NAMED_UNIT(*)
SI_UNIT(.CENTI.,.METRE.)
);
#23731=(
NAMED_UNIT(*)
PLANE_ANGLE_UNIT()
SI_UNIT($,.RADIAN.)
);
#23732=(
NAMED_UNIT(*)
SI_UNIT($,.STERADIAN.)
SOLID_ANGLE_UNIT()
);
#23800=SHAPE_DEFINITION_REPRESENTATION(#23916,#24179);
#23916=PRODUCT_DEFINITION_SHAPE('',$,#24296);
#24179=SHAPE_REPRESENTATION('',(#14672),#23679);
#24228=PRODUCT_DEFINITION_CONTEXT('part definition',#24578,'design');
#24296=PRODUCT_DEFINITION('M4 short cap screw (24)',
'M4 short cap screw (24)',#24412,#24228);
#24412=PRODUCT_DEFINITION_FORMATION('',$,#24647);
#24578=APPLICATION_CONTEXT(
'Core Data for Automotive Mechanical Design Process');
#24579=PRODUCT_CONTEXT('part definition',#24578,'mechanical');
#24647=PRODUCT('M4 short cap screw (24)','M4 short cap screw (24)',
'M4 short cap screw (24)',(#24579));
#24766=COLOUR_RGB('Black',0.12,0.14,0.17);
#24767=FILL_AREA_STYLE_COLOUR('',#24766);
#24768=FILL_AREA_STYLE('',(#24767));
#24769=SURFACE_STYLE_FILL_AREA(#24768);
#24770=SURFACE_SIDE_STYLE('',(#24769));
#24771=SURFACE_STYLE_USAGE(.BOTH.,#24770);
#24772=PRESENTATION_STYLE_ASSIGNMENT((#24771));
ENDSEC;
END-ISO-10303-21;
